ISO-10303-21;
HEADER;
/* Generated by software containing ST-Developer
 * from STEP Tools, Inc. (www.steptools.com) 
 */

FILE_DESCRIPTION(
/* description */ ('PAT-082'),
/* implementation_level */ '2;1');

FILE_NAME(
/* name */ 'Cover gasket.step',
/* time_stamp */ '2026-10-29T20:16:13-07:00',
/* author */ (''),
/* organization */ (''),
/* preprocessor_version */ 'ST-DEVELOPER v20.2',
/* originating_system */ 'Autodesk Translation Framework v15.17.0.0',
/* authorisation */ '');

FILE_SCHEMA (('AUTOMOTIVE_DESIGN { 1 0 10303 214 3 1 1 }'));
ENDSEC;

DATA;
#10=MECHANICAL_DESIGN_GEOMETRIC_PRESENTATION_REPRESENTATION('',(#247),#8266);
#203=SHAPE_REPRESENTATION_RELATIONSHIP('SRR','None',#8365,#225);
#225=ADVANCED_BREP_SHAPE_REPRESENTATION('',(#269),#8249);
#247=STYLED_ITEM('',(#8530),#269);
#269=MANIFOLD_SOLID_BREP('Body1',#4587);
#334=FACE_BOUND('',#987,.T.);
#335=FACE_BOUND('',#988,.T.);
#336=FACE_BOUND('',#989,.T.);
#337=FACE_BOUND('',#990,.T.);
#338=FACE_BOUND('',#991,.T.);
#339=FACE_BOUND('',#992,.T.);
#340=FACE_BOUND('',#993,.T.);
#341=FACE_BOUND('',#994,.T.);
#342=FACE_BOUND('',#995,.T.);
#343=FACE_BOUND('',#997,.T.);
#344=FACE_BOUND('',#998,.T.);
#345=FACE_BOUND('',#999,.T.);
#346=FACE_BOUND('',#1000,.T.);
#347=FACE_BOUND('',#1001,.T.);
#348=FACE_BOUND('',#1002,.T.);
#349=FACE_BOUND('',#1003,.T.);
#350=FACE_BOUND('',#1004,.T.);
#351=FACE_BOUND('',#1005,.T.);
#449=PLANE('',#5029);
#450=PLANE('',#5030);
#451=PLANE('',#5031);
#452=PLANE('',#5032);
#453=PLANE('',#5033);
#454=PLANE('',#5034);
#455=PLANE('',#5035);
#456=PLANE('',#5036);
#457=PLANE('',#5037);
#458=PLANE('',#5038);
#648=FACE_OUTER_BOUND('',#970,.T.);
#649=FACE_OUTER_BOUND('',#971,.T.);
#650=FACE_OUTER_BOUND('',#972,.T.);
#651=FACE_OUTER_BOUND('',#973,.T.);
#652=FACE_OUTER_BOUND('',#974,.T.);
#653=FACE_OUTER_BOUND('',#975,.T.);
#654=FACE_OUTER_BOUND('',#976,.T.);
#655=FACE_OUTER_BOUND('',#977,.T.);
#656=FACE_OUTER_BOUND('',#978,.T.);
#657=FACE_OUTER_BOUND('',#979,.T.);
#658=FACE_OUTER_BOUND('',#980,.T.);
#659=FACE_OUTER_BOUND('',#981,.T.);
#660=FACE_OUTER_BOUND('',#982,.T.);
#661=FACE_OUTER_BOUND('',#983,.T.);
#662=FACE_OUTER_BOUND('',#984,.T.);
#663=FACE_OUTER_BOUND('',#985,.T.);
#664=FACE_OUTER_BOUND('',#986,.T.);
#665=FACE_OUTER_BOUND('',#996,.T.);
#970=EDGE_LOOP('',(#3446,#3447,#3448,#3449));
#971=EDGE_LOOP('',(#3450,#3451,#3452,#3453));
#972=EDGE_LOOP('',(#3454,#3455,#3456,#3457));
#973=EDGE_LOOP('',(#3458,#3459,#3460,#3461));
#974=EDGE_LOOP('',(#3462,#3463,#3464,#3465));
#975=EDGE_LOOP('',(#3466,#3467,#3468,#3469));
#976=EDGE_LOOP('',(#3470,#3471,#3472,#3473));
#977=EDGE_LOOP('',(#3474,#3475,#3476,#3477));
#978=EDGE_LOOP('',(#3478,#3479,#3480,#3481));
#979=EDGE_LOOP('',(#3482,#3483,#3484,#3485));
#980=EDGE_LOOP('',(#3486,#3487,#3488,#3489));
#981=EDGE_LOOP('',(#3490,#3491,#3492,#3493));
#982=EDGE_LOOP('',(#3494,#3495,#3496,#3497));
#983=EDGE_LOOP('',(#3498,#3499,#3500,#3501));
#984=EDGE_LOOP('',(#3502,#3503,#3504,#3505));
#985=EDGE_LOOP('',(#3506,#3507,#3508,#3509));
#986=EDGE_LOOP('',(#3510,#3511,#3512,#3513));
#987=EDGE_LOOP('',(#3514));
#988=EDGE_LOOP('',(#3515,#3516,#3517,#3518));
#989=EDGE_LOOP('',(#3519));
#990=EDGE_LOOP('',(#3520));
#991=EDGE_LOOP('',(#3521));
#992=EDGE_LOOP('',(#3522));
#993=EDGE_LOOP('',(#3523));
#994=EDGE_LOOP('',(#3524));
#995=EDGE_LOOP('',(#3525));
#996=EDGE_LOOP('',(#3526,#3527,#3528,#3529));
#997=EDGE_LOOP('',(#3530));
#998=EDGE_LOOP('',(#3531,#3532,#3533,#3534));
#999=EDGE_LOOP('',(#3535));
#1000=EDGE_LOOP('',(#3536));
#1001=EDGE_LOOP('',(#3537));
#1002=EDGE_LOOP('',(#3538));
#1003=EDGE_LOOP('',(#3539));
#1004=EDGE_LOOP('',(#3540));
#1005=EDGE_LOOP('',(#3541));
#1343=LINE('',#7191,#1698);
#1344=LINE('',#7197,#1699);
#1345=LINE('',#7203,#1700);
#1346=LINE('',#7209,#1701);
#1347=LINE('',#7215,#1702);
#1348=LINE('',#7221,#1703);
#1349=LINE('',#7227,#1704);
#1350=LINE('',#7233,#1705);
#1351=LINE('',#7238,#1706);
#1352=LINE('',#7240,#1707);
#1353=LINE('',#7242,#1708);
#1354=LINE('',#7243,#1709);
#1355=LINE('',#7246,#1710);
#1356=LINE('',#7248,#1711);
#1357=LINE('',#7249,#1712);
#1358=LINE('',#7252,#1713);
#1359=LINE('',#7254,#1714);
#1360=LINE('',#7255,#1715);
#1361=LINE('',#7257,#1716);
#1362=LINE('',#7258,#1717);
#1363=LINE('',#7262,#1718);
#1364=LINE('',#7264,#1719);
#1365=LINE('',#7266,#1720);
#1366=LINE('',#7267,#1721);
#1367=LINE('',#7270,#1722);
#1368=LINE('',#7272,#1723);
#1369=LINE('',#7273,#1724);
#1370=LINE('',#7276,#1725);
#1371=LINE('',#7278,#1726);
#1372=LINE('',#7279,#1727);
#1373=LINE('',#7281,#1728);
#1374=LINE('',#7282,#1729);
#1698=VECTOR('',#5806,0.15);
#1699=VECTOR('',#5813,0.15);
#1700=VECTOR('',#5820,0.225);
#1701=VECTOR('',#5827,0.225);
#1702=VECTOR('',#5834,0.225);
#1703=VECTOR('',#5841,0.225);
#1704=VECTOR('',#5848,0.225);
#1705=VECTOR('',#5855,0.225);
#1706=VECTOR('',#5860,1.);
#1707=VECTOR('',#5861,1.);
#1708=VECTOR('',#5862,1.);
#1709=VECTOR('',#5863,1.);
#1710=VECTOR('',#5866,1.);
#1711=VECTOR('',#5867,1.);
#1712=VECTOR('',#5868,1.);
#1713=VECTOR('',#5871,1.);
#1714=VECTOR('',#5872,1.);
#1715=VECTOR('',#5873,1.);
#1716=VECTOR('',#5876,1.);
#1717=VECTOR('',#5877,1.);
#1718=VECTOR('',#5880,1.);
#1719=VECTOR('',#5881,1.);
#1720=VECTOR('',#5882,1.);
#1721=VECTOR('',#5883,1.);
#1722=VECTOR('',#5886,1.);
#1723=VECTOR('',#5887,1.);
#1724=VECTOR('',#5888,1.);
#1725=VECTOR('',#5891,1.);
#1726=VECTOR('',#5892,1.);
#1727=VECTOR('',#5893,1.);
#1728=VECTOR('',#5896,1.);
#1729=VECTOR('',#5897,1.);
#2017=CIRCLE('',#5006,0.15);
#2018=CIRCLE('',#5007,0.15);
#2019=CIRCLE('',#5009,0.15);
#2020=CIRCLE('',#5010,0.15);
#2021=CIRCLE('',#5012,0.225);
#2022=CIRCLE('',#5013,0.225);
#2023=CIRCLE('',#5015,0.225);
#2024=CIRCLE('',#5016,0.225);
#2025=CIRCLE('',#5018,0.225);
#2026=CIRCLE('',#5019,0.225);
#2027=CIRCLE('',#5021,0.225);
#2028=CIRCLE('',#5022,0.225);
#2029=CIRCLE('',#5024,0.225);
#2030=CIRCLE('',#5025,0.225);
#2031=CIRCLE('',#5027,0.225);
#2032=CIRCLE('',#5028,0.225);
#2265=VERTEX_POINT('',#7188);
#2266=VERTEX_POINT('',#7190);
#2267=VERTEX_POINT('',#7194);
#2268=VERTEX_POINT('',#7196);
#2269=VERTEX_POINT('',#7200);
#2270=VERTEX_POINT('',#7202);
#2271=VERTEX_POINT('',#7206);
#2272=VERTEX_POINT('',#7208);
#2273=VERTEX_POINT('',#7212);
#2274=VERTEX_POINT('',#7214);
#2275=VERTEX_POINT('',#7218);
#2276=VERTEX_POINT('',#7220);
#2277=VERTEX_POINT('',#7224);
#2278=VERTEX_POINT('',#7226);
#2279=VERTEX_POINT('',#7230);
#2280=VERTEX_POINT('',#7232);
#2281=VERTEX_POINT('',#7236);
#2282=VERTEX_POINT('',#7237);
#2283=VERTEX_POINT('',#7239);
#2284=VERTEX_POINT('',#7241);
#2285=VERTEX_POINT('',#7245);
#2286=VERTEX_POINT('',#7247);
#2287=VERTEX_POINT('',#7251);
#2288=VERTEX_POINT('',#7253);
#2289=VERTEX_POINT('',#7260);
#2290=VERTEX_POINT('',#7261);
#2291=VERTEX_POINT('',#7263);
#2292=VERTEX_POINT('',#7265);
#2293=VERTEX_POINT('',#7269);
#2294=VERTEX_POINT('',#7271);
#2295=VERTEX_POINT('',#7275);
#2296=VERTEX_POINT('',#7277);
#2699=EDGE_CURVE('',#2265,#2265,#2017,.T.);
#2700=EDGE_CURVE('',#2265,#2266,#1343,.T.);
#2701=EDGE_CURVE('',#2266,#2266,#2018,.T.);
#2702=EDGE_CURVE('',#2267,#2267,#2019,.T.);
#2703=EDGE_CURVE('',#2267,#2268,#1344,.T.);
#2704=EDGE_CURVE('',#2268,#2268,#2020,.T.);
#2705=EDGE_CURVE('',#2269,#2269,#2021,.T.);
#2706=EDGE_CURVE('',#2269,#2270,#1345,.T.);
#2707=EDGE_CURVE('',#2270,#2270,#2022,.T.);
#2708=EDGE_CURVE('',#2271,#2271,#2023,.T.);
#2709=EDGE_CURVE('',#2271,#2272,#1346,.T.);
#2710=EDGE_CURVE('',#2272,#2272,#2024,.T.);
#2711=EDGE_CURVE('',#2273,#2273,#2025,.T.);
#2712=EDGE_CURVE('',#2273,#2274,#1347,.T.);
#2713=EDGE_CURVE('',#2274,#2274,#2026,.T.);
#2714=EDGE_CURVE('',#2275,#2275,#2027,.T.);
#2715=EDGE_CURVE('',#2275,#2276,#1348,.T.);
#2716=EDGE_CURVE('',#2276,#2276,#2028,.T.);
#2717=EDGE_CURVE('',#2277,#2277,#2029,.T.);
#2718=EDGE_CURVE('',#2277,#2278,#1349,.T.);
#2719=EDGE_CURVE('',#2278,#2278,#2030,.T.);
#2720=EDGE_CURVE('',#2279,#2279,#2031,.T.);
#2721=EDGE_CURVE('',#2279,#2280,#1350,.T.);
#2722=EDGE_CURVE('',#2280,#2280,#2032,.T.);
#2723=EDGE_CURVE('',#2281,#2282,#1351,.T.);
#2724=EDGE_CURVE('',#2283,#2281,#1352,.T.);
#2725=EDGE_CURVE('',#2284,#2283,#1353,.T.);
#2726=EDGE_CURVE('',#2284,#2282,#1354,.T.);
#2727=EDGE_CURVE('',#2282,#2285,#1355,.T.);
#2728=EDGE_CURVE('',#2286,#2284,#1356,.T.);
#2729=EDGE_CURVE('',#2286,#2285,#1357,.T.);
#2730=EDGE_CURVE('',#2285,#2287,#1358,.T.);
#2731=EDGE_CURVE('',#2288,#2286,#1359,.T.);
#2732=EDGE_CURVE('',#2288,#2287,#1360,.T.);
#2733=EDGE_CURVE('',#2287,#2281,#1361,.T.);
#2734=EDGE_CURVE('',#2283,#2288,#1362,.T.);
#2735=EDGE_CURVE('',#2289,#2290,#1363,.T.);
#2736=EDGE_CURVE('',#2290,#2291,#1364,.T.);
#2737=EDGE_CURVE('',#2292,#2291,#1365,.T.);
#2738=EDGE_CURVE('',#2289,#2292,#1366,.T.);
#2739=EDGE_CURVE('',#2293,#2289,#1367,.T.);
#2740=EDGE_CURVE('',#2294,#2292,#1368,.T.);
#2741=EDGE_CURVE('',#2293,#2294,#1369,.T.);
#2742=EDGE_CURVE('',#2295,#2293,#1370,.T.);
#2743=EDGE_CURVE('',#2296,#2294,#1371,.T.);
#2744=EDGE_CURVE('',#2295,#2296,#1372,.T.);
#2745=EDGE_CURVE('',#2290,#2295,#1373,.T.);
#2746=EDGE_CURVE('',#2291,#2296,#1374,.T.);
#3446=ORIENTED_EDGE('',*,*,#2699,.F.);
#3447=ORIENTED_EDGE('',*,*,#2700,.T.);
#3448=ORIENTED_EDGE('',*,*,#2701,.F.);
#3449=ORIENTED_EDGE('',*,*,#2700,.F.);
#3450=ORIENTED_EDGE('',*,*,#2702,.F.);
#3451=ORIENTED_EDGE('',*,*,#2703,.T.);
#3452=ORIENTED_EDGE('',*,*,#2704,.F.);
#3453=ORIENTED_EDGE('',*,*,#2703,.F.);
#3454=ORIENTED_EDGE('',*,*,#2705,.F.);
#3455=ORIENTED_EDGE('',*,*,#2706,.T.);
#3456=ORIENTED_EDGE('',*,*,#2707,.F.);
#3457=ORIENTED_EDGE('',*,*,#2706,.F.);
#3458=ORIENTED_EDGE('',*,*,#2708,.F.);
#3459=ORIENTED_EDGE('',*,*,#2709,.T.);
#3460=ORIENTED_EDGE('',*,*,#2710,.F.);
#3461=ORIENTED_EDGE('',*,*,#2709,.F.);
#3462=ORIENTED_EDGE('',*,*,#2711,.F.);
#3463=ORIENTED_EDGE('',*,*,#2712,.T.);
#3464=ORIENTED_EDGE('',*,*,#2713,.F.);
#3465=ORIENTED_EDGE('',*,*,#2712,.F.);
#3466=ORIENTED_EDGE('',*,*,#2714,.F.);
#3467=ORIENTED_EDGE('',*,*,#2715,.T.);
#3468=ORIENTED_EDGE('',*,*,#2716,.F.);
#3469=ORIENTED_EDGE('',*,*,#2715,.F.);
#3470=ORIENTED_EDGE('',*,*,#2717,.F.);
#3471=ORIENTED_EDGE('',*,*,#2718,.T.);
#3472=ORIENTED_EDGE('',*,*,#2719,.F.);
#3473=ORIENTED_EDGE('',*,*,#2718,.F.);
#3474=ORIENTED_EDGE('',*,*,#2720,.F.);
#3475=ORIENTED_EDGE('',*,*,#2721,.T.);
#3476=ORIENTED_EDGE('',*,*,#2722,.F.);
#3477=ORIENTED_EDGE('',*,*,#2721,.F.);
#3478=ORIENTED_EDGE('',*,*,#2723,.F.);
#3479=ORIENTED_EDGE('',*,*,#2724,.F.);
#3480=ORIENTED_EDGE('',*,*,#2725,.F.);
#3481=ORIENTED_EDGE('',*,*,#2726,.T.);
#3482=ORIENTED_EDGE('',*,*,#2727,.F.);
#3483=ORIENTED_EDGE('',*,*,#2726,.F.);
#3484=ORIENTED_EDGE('',*,*,#2728,.F.);
#3485=ORIENTED_EDGE('',*,*,#2729,.T.);
#3486=ORIENTED_EDGE('',*,*,#2730,.F.);
#3487=ORIENTED_EDGE('',*,*,#2729,.F.);
#3488=ORIENTED_EDGE('',*,*,#2731,.F.);
#3489=ORIENTED_EDGE('',*,*,#2732,.T.);
#3490=ORIENTED_EDGE('',*,*,#2733,.F.);
#3491=ORIENTED_EDGE('',*,*,#2732,.F.);
#3492=ORIENTED_EDGE('',*,*,#2734,.F.);
#3493=ORIENTED_EDGE('',*,*,#2724,.T.);
#3494=ORIENTED_EDGE('',*,*,#2735,.T.);
#3495=ORIENTED_EDGE('',*,*,#2736,.T.);
#3496=ORIENTED_EDGE('',*,*,#2737,.F.);
#3497=ORIENTED_EDGE('',*,*,#2738,.F.);
#3498=ORIENTED_EDGE('',*,*,#2739,.T.);
#3499=ORIENTED_EDGE('',*,*,#2738,.T.);
#3500=ORIENTED_EDGE('',*,*,#2740,.F.);
#3501=ORIENTED_EDGE('',*,*,#2741,.F.);
#3502=ORIENTED_EDGE('',*,*,#2742,.T.);
#3503=ORIENTED_EDGE('',*,*,#2741,.T.);
#3504=ORIENTED_EDGE('',*,*,#2743,.F.);
#3505=ORIENTED_EDGE('',*,*,#2744,.F.);
#3506=ORIENTED_EDGE('',*,*,#2745,.T.);
#3507=ORIENTED_EDGE('',*,*,#2744,.T.);
#3508=ORIENTED_EDGE('',*,*,#2746,.F.);
#3509=ORIENTED_EDGE('',*,*,#2736,.F.);
#3510=ORIENTED_EDGE('',*,*,#2746,.T.);
#3511=ORIENTED_EDGE('',*,*,#2743,.T.);
#3512=ORIENTED_EDGE('',*,*,#2740,.T.);
#3513=ORIENTED_EDGE('',*,*,#2737,.T.);
#3514=ORIENTED_EDGE('',*,*,#2704,.T.);
#3515=ORIENTED_EDGE('',*,*,#2730,.T.);
#3516=ORIENTED_EDGE('',*,*,#2733,.T.);
#3517=ORIENTED_EDGE('',*,*,#2723,.T.);
#3518=ORIENTED_EDGE('',*,*,#2727,.T.);
#3519=ORIENTED_EDGE('',*,*,#2722,.T.);
#3520=ORIENTED_EDGE('',*,*,#2719,.T.);
#3521=ORIENTED_EDGE('',*,*,#2716,.T.);
#3522=ORIENTED_EDGE('',*,*,#2713,.T.);
#3523=ORIENTED_EDGE('',*,*,#2710,.T.);
#3524=ORIENTED_EDGE('',*,*,#2707,.T.);
#3525=ORIENTED_EDGE('',*,*,#2701,.T.);
#3526=ORIENTED_EDGE('',*,*,#2745,.F.);
#3527=ORIENTED_EDGE('',*,*,#2735,.F.);
#3528=ORIENTED_EDGE('',*,*,#2739,.F.);
#3529=ORIENTED_EDGE('',*,*,#2742,.F.);
#3530=ORIENTED_EDGE('',*,*,#2702,.T.);
#3531=ORIENTED_EDGE('',*,*,#2731,.T.);
#3532=ORIENTED_EDGE('',*,*,#2728,.T.);
#3533=ORIENTED_EDGE('',*,*,#2725,.T.);
#3534=ORIENTED_EDGE('',*,*,#2734,.T.);
#3535=ORIENTED_EDGE('',*,*,#2720,.T.);
#3536=ORIENTED_EDGE('',*,*,#2717,.T.);
#3537=ORIENTED_EDGE('',*,*,#2714,.T.);
#3538=ORIENTED_EDGE('',*,*,#2711,.T.);
#3539=ORIENTED_EDGE('',*,*,#2708,.T.);
#3540=ORIENTED_EDGE('',*,*,#2705,.T.);
#3541=ORIENTED_EDGE('',*,*,#2699,.T.);
#4252=CYLINDRICAL_SURFACE('',#5005,0.15);
#4253=CYLINDRICAL_SURFACE('',#5008,0.15);
#4254=CYLINDRICAL_SURFACE('',#5011,0.225);
#4255=CYLINDRICAL_SURFACE('',#5014,0.225);
#4256=CYLINDRICAL_SURFACE('',#5017,0.225);
#4257=CYLINDRICAL_SURFACE('',#5020,0.225);
#4258=CYLINDRICAL_SURFACE('',#5023,0.225);
#4259=CYLINDRICAL_SURFACE('',#5026,0.225);
#4387=ADVANCED_FACE('',(#648),#4252,.F.);
#4388=ADVANCED_FACE('',(#649),#4253,.F.);
#4389=ADVANCED_FACE('',(#650),#4254,.F.);
#4390=ADVANCED_FACE('',(#651),#4255,.F.);
#4391=ADVANCED_FACE('',(#652),#4256,.F.);
#4392=ADVANCED_FACE('',(#653),#4257,.F.);
#4393=ADVANCED_FACE('',(#654),#4258,.F.);
#4394=ADVANCED_FACE('',(#655),#4259,.F.);
#4395=ADVANCED_FACE('',(#656),#449,.F.);
#4396=ADVANCED_FACE('',(#657),#450,.F.);
#4397=ADVANCED_FACE('',(#658),#451,.F.);
#4398=ADVANCED_FACE('',(#659),#452,.F.);
#4399=ADVANCED_FACE('',(#660),#453,.T.);
#4400=ADVANCED_FACE('',(#661),#454,.T.);
#4401=ADVANCED_FACE('',(#662),#455,.T.);
#4402=ADVANCED_FACE('',(#663),#456,.T.);
#4403=ADVANCED_FACE('',(#664,#334,#335,#336,#337,#338,#339,#340,#341,#342),
#457,.T.);
#4404=ADVANCED_FACE('',(#665,#343,#344,#345,#346,#347,#348,#349,#350,#351),
#458,.F.);
#4587=CLOSED_SHELL('',(#4387,#4388,#4389,#4390,#4391,#4392,#4393,#4394,
#4395,#4396,#4397,#4398,#4399,#4400,#4401,#4402,#4403,#4404));
#5004=AXIS2_PLACEMENT_3D('',#7186,#5800,#5801);
#5005=AXIS2_PLACEMENT_3D('',#7187,#5802,#5803);
#5006=AXIS2_PLACEMENT_3D('',#7189,#5804,#5805);
#5007=AXIS2_PLACEMENT_3D('',#7192,#5807,#5808);
#5008=AXIS2_PLACEMENT_3D('',#7193,#5809,#5810);
#5009=AXIS2_PLACEMENT_3D('',#7195,#5811,#5812);
#5010=AXIS2_PLACEMENT_3D('',#7198,#5814,#5815);
#5011=AXIS2_PLACEMENT_3D('',#7199,#5816,#5817);
#5012=AXIS2_PLACEMENT_3D('',#7201,#5818,#5819);
#5013=AXIS2_PLACEMENT_3D('',#7204,#5821,#5822);
#5014=AXIS2_PLACEMENT_3D('',#7205,#5823,#5824);
#5015=AXIS2_PLACEMENT_3D('',#7207,#5825,#5826);
#5016=AXIS2_PLACEMENT_3D('',#7210,#5828,#5829);
#5017=AXIS2_PLACEMENT_3D('',#7211,#5830,#5831);
#5018=AXIS2_PLACEMENT_3D('',#7213,#5832,#5833);
#5019=AXIS2_PLACEMENT_3D('',#7216,#5835,#5836);
#5020=AXIS2_PLACEMENT_3D('',#7217,#5837,#5838);
#5021=AXIS2_PLACEMENT_3D('',#7219,#5839,#5840);
#5022=AXIS2_PLACEMENT_3D('',#7222,#5842,#5843);
#5023=AXIS2_PLACEMENT_3D('',#7223,#5844,#5845);
#5024=AXIS2_PLACEMENT_3D('',#7225,#5846,#5847);
#5025=AXIS2_PLACEMENT_3D('',#7228,#5849,#5850);
#5026=AXIS2_PLACEMENT_3D('',#7229,#5851,#5852);
#5027=AXIS2_PLACEMENT_3D('',#7231,#5853,#5854);
#5028=AXIS2_PLACEMENT_3D('',#7234,#5856,#5857);
#5029=AXIS2_PLACEMENT_3D('',#7235,#5858,#5859);
#5030=AXIS2_PLACEMENT_3D('',#7244,#5864,#5865);
#5031=AXIS2_PLACEMENT_3D('',#7250,#5869,#5870);
#5032=AXIS2_PLACEMENT_3D('',#7256,#5874,#5875);
#5033=AXIS2_PLACEMENT_3D('',#7259,#5878,#5879);
#5034=AXIS2_PLACEMENT_3D('',#7268,#5884,#5885);
#5035=AXIS2_PLACEMENT_3D('',#7274,#5889,#5890);
#5036=AXIS2_PLACEMENT_3D('',#7280,#5894,#5895);
#5037=AXIS2_PLACEMENT_3D('',#7283,#5898,#5899);
#5038=AXIS2_PLACEMENT_3D('',#7284,#5900,#5901);
#5800=DIRECTION('axis',(0.,0.,1.));
#5801=DIRECTION('refdir',(1.,0.,0.));
#5802=DIRECTION('center_axis',(0.,0.,1.));
#5803=DIRECTION('ref_axis',(1.,0.,0.));
#5804=DIRECTION('center_axis',(0.,0.,1.));
#5805=DIRECTION('ref_axis',(1.,0.,0.));
#5806=DIRECTION('',(0.,0.,1.));
#5807=DIRECTION('center_axis',(0.,0.,-1.));
#5808=DIRECTION('ref_axis',(1.,0.,0.));
#5809=DIRECTION('center_axis',(0.,0.,1.));
#5810=DIRECTION('ref_axis',(1.,0.,0.));
#5811=DIRECTION('center_axis',(0.,0.,1.));
#5812=DIRECTION('ref_axis',(1.,0.,0.));
#5813=DIRECTION('',(0.,0.,1.));
#5814=DIRECTION('center_axis',(0.,0.,-1.));
#5815=DIRECTION('ref_axis',(1.,0.,0.));
#5816=DIRECTION('center_axis',(0.,0.,1.));
#5817=DIRECTION('ref_axis',(1.,0.,0.));
#5818=DIRECTION('center_axis',(0.,0.,1.));
#5819=DIRECTION('ref_axis',(1.,0.,0.));
#5820=DIRECTION('',(0.,0.,1.));
#5821=DIRECTION('center_axis',(0.,0.,-1.));
#5822=DIRECTION('ref_axis',(1.,0.,0.));
#5823=DIRECTION('center_axis',(0.,0.,1.));
#5824=DIRECTION('ref_axis',(1.,0.,0.));
#5825=DIRECTION('center_axis',(0.,0.,1.));
#5826=DIRECTION('ref_axis',(1.,0.,0.));
#5827=DIRECTION('',(0.,0.,1.));
#5828=DIRECTION('center_axis',(0.,0.,-1.));
#5829=DIRECTION('ref_axis',(1.,0.,0.));
#5830=DIRECTION('center_axis',(0.,0.,1.));
#5831=DIRECTION('ref_axis',(1.,0.,0.));
#5832=DIRECTION('center_axis',(0.,0.,1.));
#5833=DIRECTION('ref_axis',(1.,0.,0.));
#5834=DIRECTION('',(0.,0.,1.));
#5835=DIRECTION('center_axis',(0.,0.,-1.));
#5836=DIRECTION('ref_axis',(1.,0.,0.));
#5837=DIRECTION('center_axis',(0.,0.,1.));
#5838=DIRECTION('ref_axis',(1.,0.,0.));
#5839=DIRECTION('center_axis',(0.,0.,1.));
#5840=DIRECTION('ref_axis',(1.,0.,0.));
#5841=DIRECTION('',(0.,0.,1.));
#5842=DIRECTION('center_axis',(0.,0.,-1.));
#5843=DIRECTION('ref_axis',(1.,0.,0.));
#5844=DIRECTION('center_axis',(0.,0.,1.));
#5845=DIRECTION('ref_axis',(1.,0.,0.));
#5846=DIRECTION('center_axis',(0.,0.,1.));
#5847=DIRECTION('ref_axis',(1.,0.,0.));
#5848=DIRECTION('',(0.,0.,1.));
#5849=DIRECTION('center_axis',(0.,0.,-1.));
#5850=DIRECTION('ref_axis',(1.,0.,0.));
#5851=DIRECTION('center_axis',(0.,0.,1.));
#5852=DIRECTION('ref_axis',(1.,0.,0.));
#5853=DIRECTION('center_axis',(0.,0.,1.));
#5854=DIRECTION('ref_axis',(1.,0.,0.));
#5855=DIRECTION('',(0.,0.,1.));
#5856=DIRECTION('center_axis',(0.,0.,-1.));
#5857=DIRECTION('ref_axis',(1.,0.,0.));
#5858=DIRECTION('center_axis',(0.,-1.,0.));
#5859=DIRECTION('ref_axis',(1.,0.,0.));
#5860=DIRECTION('',(-1.,0.,0.));
#5861=DIRECTION('',(0.,0.,1.));
#5862=DIRECTION('',(1.,0.,0.));
#5863=DIRECTION('',(0.,0.,1.));
#5864=DIRECTION('center_axis',(-1.,0.,0.));
#5865=DIRECTION('ref_axis',(0.,-1.,0.));
#5866=DIRECTION('',(0.,1.,0.));
#5867=DIRECTION('',(0.,-1.,0.));
#5868=DIRECTION('',(0.,0.,1.));
#5869=DIRECTION('center_axis',(0.,1.,0.));
#5870=DIRECTION('ref_axis',(-1.,0.,0.));
#5871=DIRECTION('',(1.,0.,0.));
#5872=DIRECTION('',(-1.,0.,0.));
#5873=DIRECTION('',(0.,0.,1.));
#5874=DIRECTION('center_axis',(1.,0.,0.));
#5875=DIRECTION('ref_axis',(0.,1.,0.));
#5876=DIRECTION('',(0.,-1.,0.));
#5877=DIRECTION('',(0.,1.,0.));
#5878=DIRECTION('center_axis',(0.,1.,0.));
#5879=DIRECTION('ref_axis',(-1.,0.,0.));
#5880=DIRECTION('',(-1.,0.,0.));
#5881=DIRECTION('',(0.,0.,1.));
#5882=DIRECTION('',(-1.,0.,0.));
#5883=DIRECTION('',(0.,0.,1.));
#5884=DIRECTION('center_axis',(1.,0.,0.));
#5885=DIRECTION('ref_axis',(0.,1.,0.));
#5886=DIRECTION('',(0.,1.,0.));
#5887=DIRECTION('',(0.,1.,0.));
#5888=DIRECTION('',(0.,0.,1.));
#5889=DIRECTION('center_axis',(0.,-1.,0.));
#5890=DIRECTION('ref_axis',(1.,0.,0.));
#5891=DIRECTION('',(1.,0.,0.));
#5892=DIRECTION('',(1.,0.,0.));
#5893=DIRECTION('',(0.,0.,1.));
#5894=DIRECTION('center_axis',(-1.,0.,0.));
#5895=DIRECTION('ref_axis',(0.,-1.,0.));
#5896=DIRECTION('',(0.,-1.,0.));
#5897=DIRECTION('',(0.,-1.,0.));
#5898=DIRECTION('center_axis',(0.,0.,1.));
#5899=DIRECTION('ref_axis',(1.,0.,0.));
#5900=DIRECTION('center_axis',(0.,0.,1.));
#5901=DIRECTION('ref_axis',(1.,0.,0.));
#7186=CARTESIAN_POINT('',(0.,0.,0.));
#7187=CARTESIAN_POINT('Origin',(5.,0.,1.3));
#7188=CARTESIAN_POINT('',(4.85,-1.83697019872103E-17,1.9));
#7189=CARTESIAN_POINT('Origin',(5.,0.,1.9));
#7190=CARTESIAN_POINT('',(4.85,1.83697019872103E-17,2.));
#7191=CARTESIAN_POINT('',(4.85,-1.83697019872103E-17,1.3));
#7192=CARTESIAN_POINT('Origin',(5.,0.,2.));
#7193=CARTESIAN_POINT('Origin',(-5.,0.,1.3));
#7194=CARTESIAN_POINT('',(-5.15,-1.83697019872103E-17,1.9));
#7195=CARTESIAN_POINT('Origin',(-5.,0.,1.9));
#7196=CARTESIAN_POINT('',(-5.15,1.83697019872103E-17,2.));
#7197=CARTESIAN_POINT('',(-5.15,-1.83697019872103E-17,1.3));
#7198=CARTESIAN_POINT('Origin',(-5.,0.,2.));
#7199=CARTESIAN_POINT('Origin',(4.5,-1.4,1.3));
#7200=CARTESIAN_POINT('',(4.275,-1.4,1.9));
#7201=CARTESIAN_POINT('Origin',(4.5,-1.4,1.9));
#7202=CARTESIAN_POINT('',(4.275,-1.4,2.));
#7203=CARTESIAN_POINT('',(4.275,-1.4,1.3));
#7204=CARTESIAN_POINT('Origin',(4.5,-1.4,2.));
#7205=CARTESIAN_POINT('Origin',(-4.5,-1.4,1.3));
#7206=CARTESIAN_POINT('',(-4.725,-1.4,1.9));
#7207=CARTESIAN_POINT('Origin',(-4.5,-1.4,1.9));
#7208=CARTESIAN_POINT('',(-4.725,-1.4,2.));
#7209=CARTESIAN_POINT('',(-4.725,-1.4,1.3));
#7210=CARTESIAN_POINT('Origin',(-4.5,-1.4,2.));
#7211=CARTESIAN_POINT('Origin',(-4.5,1.4,1.3));
#7212=CARTESIAN_POINT('',(-4.725,1.4,1.9));
#7213=CARTESIAN_POINT('Origin',(-4.5,1.4,1.9));
#7214=CARTESIAN_POINT('',(-4.725,1.4,2.));
#7215=CARTESIAN_POINT('',(-4.725,1.4,1.3));
#7216=CARTESIAN_POINT('Origin',(-4.5,1.4,2.));
#7217=CARTESIAN_POINT('Origin',(0.,-1.4,1.3));
#7218=CARTESIAN_POINT('',(-0.225,-1.4,1.9));
#7219=CARTESIAN_POINT('Origin',(0.,-1.4,1.9));
#7220=CARTESIAN_POINT('',(-0.225,-1.4,2.));
#7221=CARTESIAN_POINT('',(-0.225,-1.4,1.3));
#7222=CARTESIAN_POINT('Origin',(0.,-1.4,2.));
#7223=CARTESIAN_POINT('Origin',(0.,1.4,1.3));
#7224=CARTESIAN_POINT('',(-0.225,1.4,1.9));
#7225=CARTESIAN_POINT('Origin',(0.,1.4,1.9));
#7226=CARTESIAN_POINT('',(-0.225,1.4,2.));
#7227=CARTESIAN_POINT('',(-0.225,1.4,1.3));
#7228=CARTESIAN_POINT('Origin',(0.,1.4,2.));
#7229=CARTESIAN_POINT('Origin',(4.5,1.4,1.3));
#7230=CARTESIAN_POINT('',(4.275,1.4,1.9));
#7231=CARTESIAN_POINT('Origin',(4.5,1.4,1.9));
#7232=CARTESIAN_POINT('',(4.275,1.4,2.));
#7233=CARTESIAN_POINT('',(4.275,1.4,1.3));
#7234=CARTESIAN_POINT('Origin',(4.5,1.4,2.));
#7235=CARTESIAN_POINT('Origin',(-4.,-0.8,1.8));
#7236=CARTESIAN_POINT('',(4.,-0.8,2.));
#7237=CARTESIAN_POINT('',(-4.,-0.8,2.));
#7238=CARTESIAN_POINT('',(-2.,-0.8,2.));
#7239=CARTESIAN_POINT('',(4.,-0.8,1.9));
#7240=CARTESIAN_POINT('',(4.,-0.8,1.8));
#7241=CARTESIAN_POINT('',(-4.,-0.8,1.9));
#7242=CARTESIAN_POINT('',(-2.,-0.8,1.9));
#7243=CARTESIAN_POINT('',(-4.,-0.8,1.8));
#7244=CARTESIAN_POINT('Origin',(-4.,0.8,1.8));
#7245=CARTESIAN_POINT('',(-4.,0.8,2.));
#7246=CARTESIAN_POINT('',(-4.,0.4,2.));
#7247=CARTESIAN_POINT('',(-4.,0.8,1.9));
#7248=CARTESIAN_POINT('',(-4.,0.4,1.9));
#7249=CARTESIAN_POINT('',(-4.,0.8,1.8));
#7250=CARTESIAN_POINT('Origin',(4.,0.8,1.8));
#7251=CARTESIAN_POINT('',(4.,0.8,2.));
#7252=CARTESIAN_POINT('',(2.,0.8,2.));
#7253=CARTESIAN_POINT('',(4.,0.8,1.9));
#7254=CARTESIAN_POINT('',(2.,0.8,1.9));
#7255=CARTESIAN_POINT('',(4.,0.8,1.8));
#7256=CARTESIAN_POINT('Origin',(4.,-0.8,1.8));
#7257=CARTESIAN_POINT('',(4.,-0.4,2.));
#7258=CARTESIAN_POINT('',(4.,-0.4,1.9));
#7259=CARTESIAN_POINT('Origin',(5.5,1.75,1.9));
#7260=CARTESIAN_POINT('',(5.5,1.75,1.9));
#7261=CARTESIAN_POINT('',(-5.5,1.75,1.9));
#7262=CARTESIAN_POINT('',(5.5,1.75,1.9));
#7263=CARTESIAN_POINT('',(-5.5,1.75,2.));
#7264=CARTESIAN_POINT('',(-5.5,1.75,1.9));
#7265=CARTESIAN_POINT('',(5.5,1.75,2.));
#7266=CARTESIAN_POINT('',(5.5,1.75,2.));
#7267=CARTESIAN_POINT('',(5.5,1.75,1.9));
#7268=CARTESIAN_POINT('Origin',(5.5,-1.75,1.9));
#7269=CARTESIAN_POINT('',(5.5,-1.75,1.9));
#7270=CARTESIAN_POINT('',(5.5,-1.75,1.9));
#7271=CARTESIAN_POINT('',(5.5,-1.75,2.));
#7272=CARTESIAN_POINT('',(5.5,-1.75,2.));
#7273=CARTESIAN_POINT('',(5.5,-1.75,1.9));
#7274=CARTESIAN_POINT('Origin',(-5.5,-1.75,1.9));
#7275=CARTESIAN_POINT('',(-5.5,-1.75,1.9));
#7276=CARTESIAN_POINT('',(-5.5,-1.75,1.9));
#7277=CARTESIAN_POINT('',(-5.5,-1.75,2.));
#7278=CARTESIAN_POINT('',(-5.5,-1.75,2.));
#7279=CARTESIAN_POINT('',(-5.5,-1.75,1.9));
#7280=CARTESIAN_POINT('Origin',(-5.5,1.75,1.9));
#7281=CARTESIAN_POINT('',(-5.5,1.75,1.9));
#7282=CARTESIAN_POINT('',(-5.5,1.75,2.));
#7283=CARTESIAN_POINT('Origin',(0.,0.,2.));
#7284=CARTESIAN_POINT('Origin',(0.,0.,1.9));
#8224=UNCERTAINTY_MEASURE_WITH_UNIT(LENGTH_MEASURE(0.001),#8267,
'DISTANCE_ACCURACY_VALUE',
'Maximum model space distance between geometric entities at asserted c
onnectivities');
#8241=UNCERTAINTY_MEASURE_WITH_UNIT(LENGTH_MEASURE(0.001),#8267,
'DISTANCE_ACCURACY_VALUE',
'Maximum model space distance between geometric entities at asserted c
onnectivities');
#8249=(
GEOMETRIC_REPRESENTATION_CONTEXT(3)
GLOBAL_UNCERTAINTY_ASSIGNED_CONTEXT((#8224))
GLOBAL_UNIT_ASSIGNED_CONTEXT((#8267,#8269,#8270))
REPRESENTATION_CONTEXT('','3D')
);
#8266=(
GEOMETRIC_REPRESENTATION_CONTEXT(3)
GLOBAL_UNCERTAINTY_ASSIGNED_CONTEXT((#8241))
GLOBAL_UNIT_ASSIGNED_CONTEXT((#8267,#8269,#8270))
REPRESENTATION_CONTEXT('','3D')
);
#8267=(
LENGTH_UNIT()
NAMED_UNIT(*)
SI_UNIT(.CENTI.,.METRE.)
);
#8269=(
NAMED_UNIT(*)
PLANE_ANGLE_UNIT()
SI_UNIT($,.RADIAN.)
);
#8270=(
NAMED_UNIT(*)
SI_UNIT($,.STERADIAN.)
SOLID_ANGLE_UNIT()
);
#8278=SHAPE_DEFINITION_REPRESENTATION(#8302,#8365);
#8302=PRODUCT_DEFINITION_SHAPE('',$,#8390);
#8365=SHAPE_REPRESENTATION('',(#5004),#8249);
#8382=PRODUCT_DEFINITION_CONTEXT('part definition',#8456,'design');
#8390=PRODUCT_DEFINITION('Cover gasket','Cover gasket',#8414,
#8382);
#8414=PRODUCT_DEFINITION_FORMATION('',$,#8465);
#8456=APPLICATION_CONTEXT(
'Core Data for Automotive Mechanical Design Process');
#8457=PRODUCT_CONTEXT('part definition',#8456,'mechanical');
#8465=PRODUCT('Cover gasket','Cover gasket','Cover gasket',
(#8457));
#8524=COLOUR_RGB('Sky Blue',0.24,0.69,0.87);
#8525=FILL_AREA_STYLE_COLOUR('',#8524);
#8526=FILL_AREA_STYLE('',(#8525));
#8527=SURFACE_STYLE_FILL_AREA(#8526);
#8528=SURFACE_SIDE_STYLE('',(#8527));
#8529=SURFACE_STYLE_USAGE(.BOTH.,#8528);
#8530=PRESENTATION_STYLE_ASSIGNMENT((#8529));
ENDSEC;
END-ISO-10303-21;
